ISO-10303-21;
HEADER;
/* Generated by software containing ST-Developer
 * from STEP Tools, Inc. (www.steptools.com) 
 */

FILE_DESCRIPTION(
/* description */ ('PAT-065'),
/* implementation_level */ '2;1');

FILE_NAME(
/* name */ 'Low-profile M5x8 gusset screw.step',
/* time_stamp */ '2026-10-28T22:09:22-07:00',
/* author */ (''),
/* organization */ (''),
/* preprocessor_version */ 'ST-DEVELOPER v20.2',
/* originating_system */ 'Autodesk Translation Framework v15.17.0.0',
/* authorisation */ '');

FILE_SCHEMA (('AUTOMOTIVE_DESIGN { 1 0 10303 214 3 1 1 }'));
ENDSEC;

DATA;
#10=MECHANICAL_DESIGN_GEOMETRIC_PRESENTATION_REPRESENTATION('',(#161),#5502);
#119=CONICAL_SURFACE('',#3449,0.41,0.785398163397448);
#120=CONICAL_SURFACE('',#3453,0.26,0.463647609000806);
#141=SHAPE_REPRESENTATION_RELATIONSHIP('SRR','None',#5558,#151);
#151=ADVANCED_BREP_SHAPE_REPRESENTATION('',(#171),#5494);
#161=STYLED_ITEM('',(#5701),#171);
#171=MANIFOLD_SOLID_BREP('Body1',#3208);
#188=FACE_BOUND('',#607,.T.);
#189=FACE_BOUND('',#611,.T.);
#274=PLANE('',#3443);
#275=PLANE('',#3445);
#276=PLANE('',#3451);
#277=PLANE('',#3456);
#278=PLANE('',#3457);
#279=PLANE('',#3458);
#280=PLANE('',#3459);
#281=PLANE('',#3460);
#282=PLANE('',#3461);
#283=PLANE('',#3462);
#420=FACE_OUTER_BOUND('',#605,.T.);
#421=FACE_OUTER_BOUND('',#606,.T.);
#422=FACE_OUTER_BOUND('',#608,.T.);
#423=FACE_OUTER_BOUND('',#609,.T.);
#424=FACE_OUTER_BOUND('',#610,.T.);
#425=FACE_OUTER_BOUND('',#612,.T.);
#426=FACE_OUTER_BOUND('',#613,.T.);
#427=FACE_OUTER_BOUND('',#614,.T.);
#428=FACE_OUTER_BOUND('',#615,.T.);
#429=FACE_OUTER_BOUND('',#616,.T.);
#430=FACE_OUTER_BOUND('',#617,.T.);
#431=FACE_OUTER_BOUND('',#618,.T.);
#432=FACE_OUTER_BOUND('',#619,.T.);
#433=FACE_OUTER_BOUND('',#620,.T.);
#605=EDGE_LOOP('',(#2632));
#606=EDGE_LOOP('',(#2633));
#607=EDGE_LOOP('',(#2634,#2635,#2636,#2637,#2638,#2639));
#608=EDGE_LOOP('',(#2640,#2641,#2642,#2643));
#609=EDGE_LOOP('',(#2644,#2645,#2646,#2647));
#610=EDGE_LOOP('',(#2648));
#611=EDGE_LOOP('',(#2649));
#612=EDGE_LOOP('',(#2650,#2651,#2652,#2653));
#613=EDGE_LOOP('',(#2654,#2655,#2656,#2657));
#614=EDGE_LOOP('',(#2658,#2659,#2660,#2661));
#615=EDGE_LOOP('',(#2662,#2663,#2664,#2665));
#616=EDGE_LOOP('',(#2666,#2667,#2668,#2669));
#617=EDGE_LOOP('',(#2670,#2671,#2672,#2673));
#618=EDGE_LOOP('',(#2674,#2675,#2676,#2677));
#619=EDGE_LOOP('',(#2678,#2679,#2680,#2681));
#620=EDGE_LOOP('',(#2682,#2683,#2684,#2685,#2686,#2687));
#920=LINE('',#5032,#1251);
#921=LINE('',#5034,#1252);
#922=LINE('',#5036,#1253);
#923=LINE('',#5038,#1254);
#924=LINE('',#5040,#1255);
#925=LINE('',#5041,#1256);
#926=LINE('',#5045,#1257);
#927=LINE('',#5049,#1258);
#928=LINE('',#5056,#1259);
#929=LINE('',#5058,#1260);
#930=LINE('',#5062,#1261);
#931=LINE('',#5063,#1262);
#932=LINE('',#5064,#1263);
#933=LINE('',#5067,#1264);
#934=LINE('',#5068,#1265);
#935=LINE('',#5071,#1266);
#936=LINE('',#5072,#1267);
#937=LINE('',#5075,#1268);
#938=LINE('',#5076,#1269);
#939=LINE('',#5079,#1270);
#940=LINE('',#5080,#1271);
#941=LINE('',#5082,#1272);
#1251=VECTOR('',#4069,1.);
#1252=VECTOR('',#4070,1.);
#1253=VECTOR('',#4071,1.);
#1254=VECTOR('',#4072,1.);
#1255=VECTOR('',#4073,1.);
#1256=VECTOR('',#4074,1.);
#1257=VECTOR('',#4079,0.425);
#1258=VECTOR('',#4084,0.41);
#1259=VECTOR('',#4093,0.26);
#1260=VECTOR('',#4096,0.25);
#1261=VECTOR('',#4099,1.);
#1262=VECTOR('',#4100,1.);
#1263=VECTOR('',#4101,1.);
#1264=VECTOR('',#4104,1.);
#1265=VECTOR('',#4105,1.);
#1266=VECTOR('',#4108,1.);
#1267=VECTOR('',#4109,1.);
#1268=VECTOR('',#4112,1.);
#1269=VECTOR('',#4113,1.);
#1270=VECTOR('',#4116,1.);
#1271=VECTOR('',#4117,1.);
#1272=VECTOR('',#4120,1.);
#1395=CIRCLE('',#3444,0.425);
#1396=CIRCLE('',#3446,0.24505);
#1397=CIRCLE('',#3448,0.425);
#1398=CIRCLE('',#3450,0.395);
#1399=CIRCLE('',#3452,0.27);
#1400=CIRCLE('',#3454,0.24505);
#1604=VERTEX_POINT('',#5025);
#1605=VERTEX_POINT('',#5028);
#1606=VERTEX_POINT('',#5030);
#1607=VERTEX_POINT('',#5031);
#1608=VERTEX_POINT('',#5033);
#1609=VERTEX_POINT('',#5035);
#1610=VERTEX_POINT('',#5037);
#1611=VERTEX_POINT('',#5039);
#1612=VERTEX_POINT('',#5043);
#1613=VERTEX_POINT('',#5047);
#1614=VERTEX_POINT('',#5051);
#1615=VERTEX_POINT('',#5054);
#1616=VERTEX_POINT('',#5060);
#1617=VERTEX_POINT('',#5061);
#1618=VERTEX_POINT('',#5066);
#1619=VERTEX_POINT('',#5070);
#1620=VERTEX_POINT('',#5074);
#1621=VERTEX_POINT('',#5078);
#1966=EDGE_CURVE('',#1604,#1604,#1395,.T.);
#1967=EDGE_CURVE('',#1605,#1605,#1396,.T.);
#1968=EDGE_CURVE('',#1606,#1607,#920,.T.);
#1969=EDGE_CURVE('',#1608,#1606,#921,.T.);
#1970=EDGE_CURVE('',#1609,#1608,#922,.T.);
#1971=EDGE_CURVE('',#1610,#1609,#923,.T.);
#1972=EDGE_CURVE('',#1611,#1610,#924,.T.);
#1973=EDGE_CURVE('',#1607,#1611,#925,.T.);
#1974=EDGE_CURVE('',#1612,#1612,#1397,.T.);
#1975=EDGE_CURVE('',#1612,#1604,#926,.T.);
#1976=EDGE_CURVE('',#1613,#1613,#1398,.T.);
#1977=EDGE_CURVE('',#1613,#1612,#927,.T.);
#1978=EDGE_CURVE('',#1614,#1614,#1399,.T.);
#1979=EDGE_CURVE('',#1615,#1615,#1400,.F.);
#1980=EDGE_CURVE('',#1615,#1614,#928,.T.);
#1981=EDGE_CURVE('',#1605,#1615,#929,.T.);
#1982=EDGE_CURVE('',#1616,#1617,#930,.T.);
#1983=EDGE_CURVE('',#1617,#1606,#931,.T.);
#1984=EDGE_CURVE('',#1616,#1607,#932,.T.);
#1985=EDGE_CURVE('',#1617,#1618,#933,.T.);
#1986=EDGE_CURVE('',#1618,#1608,#934,.T.);
#1987=EDGE_CURVE('',#1618,#1619,#935,.T.);
#1988=EDGE_CURVE('',#1619,#1609,#936,.T.);
#1989=EDGE_CURVE('',#1619,#1620,#937,.T.);
#1990=EDGE_CURVE('',#1620,#1610,#938,.T.);
#1991=EDGE_CURVE('',#1620,#1621,#939,.T.);
#1992=EDGE_CURVE('',#1621,#1611,#940,.T.);
#1993=EDGE_CURVE('',#1621,#1616,#941,.T.);
#2632=ORIENTED_EDGE('',*,*,#1966,.F.);
#2633=ORIENTED_EDGE('',*,*,#1967,.F.);
#2634=ORIENTED_EDGE('',*,*,#1968,.F.);
#2635=ORIENTED_EDGE('',*,*,#1969,.F.);
#2636=ORIENTED_EDGE('',*,*,#1970,.F.);
#2637=ORIENTED_EDGE('',*,*,#1971,.F.);
#2638=ORIENTED_EDGE('',*,*,#1972,.F.);
#2639=ORIENTED_EDGE('',*,*,#1973,.F.);
#2640=ORIENTED_EDGE('',*,*,#1974,.F.);
#2641=ORIENTED_EDGE('',*,*,#1975,.T.);
#2642=ORIENTED_EDGE('',*,*,#1966,.T.);
#2643=ORIENTED_EDGE('',*,*,#1975,.F.);
#2644=ORIENTED_EDGE('',*,*,#1976,.F.);
#2645=ORIENTED_EDGE('',*,*,#1977,.T.);
#2646=ORIENTED_EDGE('',*,*,#1974,.T.);
#2647=ORIENTED_EDGE('',*,*,#1977,.F.);
#2648=ORIENTED_EDGE('',*,*,#1976,.T.);
#2649=ORIENTED_EDGE('',*,*,#1978,.F.);
#2650=ORIENTED_EDGE('',*,*,#1979,.F.);
#2651=ORIENTED_EDGE('',*,*,#1980,.T.);
#2652=ORIENTED_EDGE('',*,*,#1978,.T.);
#2653=ORIENTED_EDGE('',*,*,#1980,.F.);
#2654=ORIENTED_EDGE('',*,*,#1967,.T.);
#2655=ORIENTED_EDGE('',*,*,#1981,.T.);
#2656=ORIENTED_EDGE('',*,*,#1979,.T.);
#2657=ORIENTED_EDGE('',*,*,#1981,.F.);
#2658=ORIENTED_EDGE('',*,*,#1982,.T.);
#2659=ORIENTED_EDGE('',*,*,#1983,.T.);
#2660=ORIENTED_EDGE('',*,*,#1968,.T.);
#2661=ORIENTED_EDGE('',*,*,#1984,.F.);
#2662=ORIENTED_EDGE('',*,*,#1985,.T.);
#2663=ORIENTED_EDGE('',*,*,#1986,.T.);
#2664=ORIENTED_EDGE('',*,*,#1969,.T.);
#2665=ORIENTED_EDGE('',*,*,#1983,.F.);
#2666=ORIENTED_EDGE('',*,*,#1987,.T.);
#2667=ORIENTED_EDGE('',*,*,#1988,.T.);
#2668=ORIENTED_EDGE('',*,*,#1970,.T.);
#2669=ORIENTED_EDGE('',*,*,#1986,.F.);
#2670=ORIENTED_EDGE('',*,*,#1989,.T.);
#2671=ORIENTED_EDGE('',*,*,#1990,.T.);
#2672=ORIENTED_EDGE('',*,*,#1971,.T.);
#2673=ORIENTED_EDGE('',*,*,#1988,.F.);
#2674=ORIENTED_EDGE('',*,*,#1991,.T.);
#2675=ORIENTED_EDGE('',*,*,#1992,.T.);
#2676=ORIENTED_EDGE('',*,*,#1972,.T.);
#2677=ORIENTED_EDGE('',*,*,#1990,.F.);
#2678=ORIENTED_EDGE('',*,*,#1993,.T.);
#2679=ORIENTED_EDGE('',*,*,#1984,.T.);
#2680=ORIENTED_EDGE('',*,*,#1973,.T.);
#2681=ORIENTED_EDGE('',*,*,#1992,.F.);
#2682=ORIENTED_EDGE('',*,*,#1993,.F.);
#2683=ORIENTED_EDGE('',*,*,#1991,.F.);
#2684=ORIENTED_EDGE('',*,*,#1989,.F.);
#2685=ORIENTED_EDGE('',*,*,#1987,.F.);
#2686=ORIENTED_EDGE('',*,*,#1985,.F.);
#2687=ORIENTED_EDGE('',*,*,#1982,.F.);
#3014=CYLINDRICAL_SURFACE('',#3447,0.425);
#3015=CYLINDRICAL_SURFACE('',#3455,0.24505);
#3114=ADVANCED_FACE('',(#420),#274,.T.);
#3115=ADVANCED_FACE('',(#421,#188),#275,.F.);
#3116=ADVANCED_FACE('',(#422),#3014,.T.);
#3117=ADVANCED_FACE('',(#423),#119,.T.);
#3118=ADVANCED_FACE('',(#424,#189),#276,.T.);
#3119=ADVANCED_FACE('',(#425),#120,.T.);
#3120=ADVANCED_FACE('',(#426),#3015,.T.);
#3121=ADVANCED_FACE('',(#427),#277,.F.);
#3122=ADVANCED_FACE('',(#428),#278,.F.);
#3123=ADVANCED_FACE('',(#429),#279,.F.);
#3124=ADVANCED_FACE('',(#430),#280,.F.);
#3125=ADVANCED_FACE('',(#431),#281,.F.);
#3126=ADVANCED_FACE('',(#432),#282,.F.);
#3127=ADVANCED_FACE('',(#433),#283,.F.);
#3208=CLOSED_SHELL('',(#3114,#3115,#3116,#3117,#3118,#3119,#3120,#3121,
#3122,#3123,#3124,#3125,#3126,#3127));
#3442=AXIS2_PLACEMENT_3D('',#5023,#4059,#4060);
#3443=AXIS2_PLACEMENT_3D('',#5024,#4061,#4062);
#3444=AXIS2_PLACEMENT_3D('',#5026,#4063,#4064);
#3445=AXIS2_PLACEMENT_3D('',#5027,#4065,#4066);
#3446=AXIS2_PLACEMENT_3D('',#5029,#4067,#4068);
#3447=AXIS2_PLACEMENT_3D('',#5042,#4075,#4076);
#3448=AXIS2_PLACEMENT_3D('',#5044,#4077,#4078);
#3449=AXIS2_PLACEMENT_3D('',#5046,#4080,#4081);
#3450=AXIS2_PLACEMENT_3D('',#5048,#4082,#4083);
#3451=AXIS2_PLACEMENT_3D('',#5050,#4085,#4086);
#3452=AXIS2_PLACEMENT_3D('',#5052,#4087,#4088);
#3453=AXIS2_PLACEMENT_3D('',#5053,#4089,#4090);
#3454=AXIS2_PLACEMENT_3D('',#5055,#4091,#4092);
#3455=AXIS2_PLACEMENT_3D('',#5057,#4094,#4095);
#3456=AXIS2_PLACEMENT_3D('',#5059,#4097,#4098);
#3457=AXIS2_PLACEMENT_3D('',#5065,#4102,#4103);
#3458=AXIS2_PLACEMENT_3D('',#5069,#4106,#4107);
#3459=AXIS2_PLACEMENT_3D('',#5073,#4110,#4111);
#3460=AXIS2_PLACEMENT_3D('',#5077,#4114,#4115);
#3461=AXIS2_PLACEMENT_3D('',#5081,#4118,#4119);
#3462=AXIS2_PLACEMENT_3D('',#5083,#4121,#4122);
#4059=DIRECTION('axis',(0.,0.,1.));
#4060=DIRECTION('refdir',(1.,0.,0.));
#4061=DIRECTION('center_axis',(0.,1.,0.));
#4062=DIRECTION('ref_axis',(1.,0.,0.));
#4063=DIRECTION('center_axis',(0.,-1.,0.));
#4064=DIRECTION('ref_axis',(1.,0.,0.));
#4065=DIRECTION('center_axis',(0.,1.,0.));
#4066=DIRECTION('ref_axis',(1.,0.,0.));
#4067=DIRECTION('center_axis',(0.,1.,0.));
#4068=DIRECTION('ref_axis',(1.,0.,0.));
#4069=DIRECTION('',(0.5,0.,0.866025403784439));
#4070=DIRECTION('',(1.,0.,1.20185167898973E-16));
#4071=DIRECTION('',(0.5,0.,-0.866025403784439));
#4072=DIRECTION('',(-0.5,0.,-0.866025403784439));
#4073=DIRECTION('',(-1.,0.,-2.40370335797945E-16));
#4074=DIRECTION('',(-0.5,0.,0.866025403784439));
#4075=DIRECTION('center_axis',(0.,-1.,0.));
#4076=DIRECTION('ref_axis',(1.,0.,0.));
#4077=DIRECTION('center_axis',(0.,-1.,0.));
#4078=DIRECTION('ref_axis',(1.,0.,0.));
#4079=DIRECTION('',(0.,1.,0.));
#4080=DIRECTION('center_axis',(0.,1.,0.));
#4081=DIRECTION('ref_axis',(1.,0.,0.));
#4082=DIRECTION('center_axis',(0.,-1.,0.));
#4083=DIRECTION('ref_axis',(1.,0.,0.));
#4084=DIRECTION('',(-0.707106781186547,0.707106781186548,-8.65956056235493E-17));
#4085=DIRECTION('center_axis',(0.,-1.,0.));
#4086=DIRECTION('ref_axis',(0.,0.,-1.));
#4087=DIRECTION('center_axis',(0.,-1.,0.));
#4088=DIRECTION('ref_axis',(1.,0.,0.));
#4089=DIRECTION('center_axis',(0.,1.,0.));
#4090=DIRECTION('ref_axis',(1.,0.,0.));
#4091=DIRECTION('center_axis',(0.,1.,0.));
#4092=DIRECTION('ref_axis',(1.,0.,0.));
#4093=DIRECTION('',(-0.447213595499958,0.894427190999916,-5.47678698264203E-17));
#4094=DIRECTION('center_axis',(0.,-1.,0.));
#4095=DIRECTION('ref_axis',(1.,0.,0.));
#4096=DIRECTION('',(0.,1.,0.));
#4097=DIRECTION('center_axis',(0.866025403784439,0.,-0.5));
#4098=DIRECTION('ref_axis',(0.5,0.,0.866025403784439));
#4099=DIRECTION('',(-0.5,0.,-0.866025403784439));
#4100=DIRECTION('',(0.,-1.,0.));
#4101=DIRECTION('',(0.,-1.,0.));
#4102=DIRECTION('center_axis',(1.20185167898973E-16,0.,-1.));
#4103=DIRECTION('ref_axis',(1.,0.,1.20185167898973E-16));
#4104=DIRECTION('',(-1.,0.,-1.20185167898973E-16));
#4105=DIRECTION('',(0.,-1.,0.));
#4106=DIRECTION('center_axis',(-0.866025403784439,0.,-0.5));
#4107=DIRECTION('ref_axis',(0.5,0.,-0.866025403784439));
#4108=DIRECTION('',(-0.5,0.,0.866025403784439));
#4109=DIRECTION('',(0.,-1.,0.));
#4110=DIRECTION('center_axis',(-0.866025403784439,0.,0.5));
#4111=DIRECTION('ref_axis',(-0.5,0.,-0.866025403784439));
#4112=DIRECTION('',(0.5,0.,0.866025403784439));
#4113=DIRECTION('',(0.,-1.,0.));
#4114=DIRECTION('center_axis',(-2.40370335797945E-16,0.,1.));
#4115=DIRECTION('ref_axis',(-1.,0.,-2.40370335797945E-16));
#4116=DIRECTION('',(1.,0.,2.40370335797945E-16));
#4117=DIRECTION('',(0.,-1.,0.));
#4118=DIRECTION('center_axis',(0.866025403784439,0.,0.5));
#4119=DIRECTION('ref_axis',(-0.5,0.,0.866025403784439));
#4120=DIRECTION('',(0.5,0.,-0.866025403784439));
#4121=DIRECTION('center_axis',(0.,1.,0.));
#4122=DIRECTION('ref_axis',(1.,0.,0.));
#5023=CARTESIAN_POINT('',(0.,0.,0.));
#5024=CARTESIAN_POINT('Origin',(0.,0.2,0.));
#5025=CARTESIAN_POINT('',(-0.425,0.2,-5.20474889637625E-17));
#5026=CARTESIAN_POINT('Origin',(0.,0.2,0.));
#5027=CARTESIAN_POINT('Origin',(0.,-0.8,0.));
#5028=CARTESIAN_POINT('',(-0.24505,-0.8,3.00099698131059E-17));
#5029=CARTESIAN_POINT('Origin',(0.,-0.8,0.));
#5030=CARTESIAN_POINT('',(0.115470053837925,-0.8,-0.2));
#5031=CARTESIAN_POINT('',(0.23094010767585,-0.8,0.));
#5032=CARTESIAN_POINT('',(0.23094010767585,-0.8,0.));
#5033=CARTESIAN_POINT('',(-0.115470053837925,-0.8,-0.2));
#5034=CARTESIAN_POINT('',(0.115470053837925,-0.8,-0.2));
#5035=CARTESIAN_POINT('',(-0.23094010767585,-0.8,-2.77555756156289E-17));
#5036=CARTESIAN_POINT('',(-0.115470053837925,-0.8,-0.2));
#5037=CARTESIAN_POINT('',(-0.115470053837925,-0.8,0.2));
#5038=CARTESIAN_POINT('',(-0.23094010767585,-0.8,-2.82820063659975E-17));
#5039=CARTESIAN_POINT('',(0.115470053837925,-0.8,0.2));
#5040=CARTESIAN_POINT('',(-0.115470053837925,-0.8,0.2));
#5041=CARTESIAN_POINT('',(0.115470053837925,-0.8,0.2));
#5042=CARTESIAN_POINT('Origin',(0.,0.24,0.));
#5043=CARTESIAN_POINT('',(-0.425,0.0299999999999998,-5.20474889637625E-17));
#5044=CARTESIAN_POINT('Origin',(0.,0.0299999999999998,0.));
#5045=CARTESIAN_POINT('',(-0.425,0.24,-5.20474889637625E-17));
#5046=CARTESIAN_POINT('Origin',(0.,0.0150000000000001,0.));
#5047=CARTESIAN_POINT('',(-0.395,4.85722573273506E-17,-4.83735485663204E-17));
#5048=CARTESIAN_POINT('Origin',(0.,0.,0.));
#5049=CARTESIAN_POINT('',(-0.41,0.0150000000000001,-5.02105187650415E-17));
#5050=CARTESIAN_POINT('Origin',(0.27,0.,0.));
#5051=CARTESIAN_POINT('',(-0.27,0.,-3.30654635769785E-17));
#5052=CARTESIAN_POINT('Origin',(0.,0.,0.));
#5053=CARTESIAN_POINT('Origin',(0.,-0.02,0.));
#5054=CARTESIAN_POINT('',(-0.24505,-0.0498999999999999,3.00099698131059E-17));
#5055=CARTESIAN_POINT('Origin',(0.,-0.0498999999999999,0.));
#5056=CARTESIAN_POINT('',(-0.26,-0.02,-3.18408167778312E-17));
#5057=CARTESIAN_POINT('Origin',(0.,-0.995,0.));
#5058=CARTESIAN_POINT('',(-0.24505,-0.995,-3.00099698131059E-17));
#5059=CARTESIAN_POINT('Origin',(0.115470053837925,-0.5,-0.2));
#5060=CARTESIAN_POINT('',(0.23094010767585,-0.5,0.));
#5061=CARTESIAN_POINT('',(0.115470053837925,-0.5,-0.2));
#5062=CARTESIAN_POINT('',(0.23094010767585,-0.5,0.));
#5063=CARTESIAN_POINT('',(0.115470053837925,-0.5,-0.2));
#5064=CARTESIAN_POINT('',(0.23094010767585,-0.5,0.));
#5065=CARTESIAN_POINT('Origin',(-0.115470053837925,-0.5,-0.2));
#5066=CARTESIAN_POINT('',(-0.115470053837925,-0.5,-0.2));
#5067=CARTESIAN_POINT('',(0.115470053837925,-0.5,-0.2));
#5068=CARTESIAN_POINT('',(-0.115470053837925,-0.5,-0.2));
#5069=CARTESIAN_POINT('Origin',(-0.23094010767585,-0.5,-2.77555756156289E-17));
#5070=CARTESIAN_POINT('',(-0.23094010767585,-0.5,-2.82820063659975E-17));
#5071=CARTESIAN_POINT('',(-0.115470053837925,-0.5,-0.2));
#5072=CARTESIAN_POINT('',(-0.23094010767585,-0.5,-2.82820063659975E-17));
#5073=CARTESIAN_POINT('Origin',(-0.115470053837925,-0.5,0.2));
#5074=CARTESIAN_POINT('',(-0.115470053837925,-0.5,0.2));
#5075=CARTESIAN_POINT('',(-0.23094010767585,-0.5,-2.82820063659975E-17));
#5076=CARTESIAN_POINT('',(-0.115470053837925,-0.5,0.2));
#5077=CARTESIAN_POINT('Origin',(0.115470053837925,-0.5,0.2));
#5078=CARTESIAN_POINT('',(0.115470053837925,-0.5,0.2));
#5079=CARTESIAN_POINT('',(-0.115470053837925,-0.5,0.2));
#5080=CARTESIAN_POINT('',(0.115470053837925,-0.5,0.2));
#5081=CARTESIAN_POINT('Origin',(0.23094010767585,-0.5,0.));
#5082=CARTESIAN_POINT('',(0.115470053837925,-0.5,0.2));
#5083=CARTESIAN_POINT('Origin',(0.,-0.5,0.));
#5481=UNCERTAINTY_MEASURE_WITH_UNIT(LENGTH_MEASURE(0.001),#5503,
'DISTANCE_ACCURACY_VALUE',
'Maximum model space distance between geometric entities at asserted c
onnectivities');
#5489=UNCERTAINTY_MEASURE_WITH_UNIT(LENGTH_MEASURE(0.001),#5503,
'DISTANCE_ACCURACY_VALUE',
'Maximum model space distance between geometric entities at asserted c
onnectivities');
#5494=(
GEOMETRIC_REPRESENTATION_CONTEXT(3)
GLOBAL_UNCERTAINTY_ASSIGNED_CONTEXT((#5481))
GLOBAL_UNIT_ASSIGNED_CONTEXT((#5503,#5505,#5506))
REPRESENTATION_CONTEXT('','3D')
);
#5502=(
GEOMETRIC_REPRESENTATION_CONTEXT(3)
GLOBAL_UNCERTAINTY_ASSIGNED_CONTEXT((#5489))
GLOBAL_UNIT_ASSIGNED_CONTEXT((#5503,#5505,#5506))
REPRESENTATION_CONTEXT('','3D')
);
#5503=(
LENGTH_UNIT()
NAMED_UNIT(*)
SI_UNIT(.CENTI.,.METRE.)
);
#5505=(
NAMED_UNIT(*)
PLANE_ANGLE_UNIT()
SI_UNIT($,.RADIAN.)
);
#5506=(
NAMED_UNIT(*)
SI_UNIT($,.STERADIAN.)
SOLID_ANGLE_UNIT()
);
#5511=SHAPE_DEFINITION_REPRESENTATION(#5523,#5558);
#5523=PRODUCT_DEFINITION_SHAPE('',$,#5571);
#5558=SHAPE_REPRESENTATION('',(#3442),#5494);
#5566=PRODUCT_DEFINITION_CONTEXT('part definition',#5604,'design');
#5571=PRODUCT_DEFINITION('Low-profile M5x8 gusset screw',
'Low-profile M5x8 gusset screw',#5583,#5566);
#5583=PRODUCT_DEFINITION_FORMATION('',$,#5610);
#5604=APPLICATION_CONTEXT(
'Core Data for Automotive Mechanical Design Process');
#5605=PRODUCT_CONTEXT('part definition',#5604,'mechanical');
#5610=PRODUCT('Low-profile M5x8 gusset screw','Low-profile M5x8 gusset screw',
'Low-profile M5x8 gusset screw',(#5605));
#5695=COLOUR_RGB('Black',0.12,0.14,0.17);
#5696=FILL_AREA_STYLE_COLOUR('',#5695);
#5697=FILL_AREA_STYLE('',(#5696));
#5698=SURFACE_STYLE_FILL_AREA(#5697);
#5699=SURFACE_SIDE_STYLE('',(#5698));
#5700=SURFACE_STYLE_USAGE(.BOTH.,#5699);
#5701=PRESENTATION_STYLE_ASSIGNMENT((#5700));
ENDSEC;
END-ISO-10303-21;
